ISO-10303-21;
HEADER;
/* Generated by software containing ST-Developer
 * from STEP Tools, Inc. (www.steptools.com) 
 */

FILE_DESCRIPTION(
/* description */ (''),
/* implementation_level */ '2;1');

FILE_NAME(
/* name */ 'Ring_01.step',
/* time_stamp */ '2026-10-05T14:32:37-07:00',
/* author */ (''),
/* organization */ (''),
/* preprocessor_version */ 'ST-DEVELOPER v20.2',
/* originating_system */ 'Autodesk Translation Framework v15.15.0.0',
/* authorisation */ '');

FILE_SCHEMA (('AUTOMOTIVE_DESIGN { 1 0 10303 214 3 1 1 }'));
ENDSEC;

DATA;
#10=MECHANICAL_DESIGN_GEOMETRIC_PRESENTATION_REPRESENTATION('',(#496),#74103);
#488=SHAPE_REPRESENTATION_RELATIONSHIP('SRR','None',#74130,#492);
#492=ADVANCED_BREP_SHAPE_REPRESENTATION('',(#500),#74101);
#496=STYLED_ITEM('',(#74158),#500);
#500=MANIFOLD_SOLID_BREP('Body1',#4575);
#522=TOROIDAL_SURFACE('',#4828,19.9,0.400000000000003);
#523=TOROIDAL_SURFACE('',#4833,20.1,0.399999999999996);
#524=TOROIDAL_SURFACE('',#4838,20.1,0.399999999999998);
#525=TOROIDAL_SURFACE('',#4843,19.9,0.400000000000003);
#582=FACE_BOUND('',#913,.T.);
#583=FACE_BOUND('',#918,.T.);
#608=PLANE('',#4831);
#609=PLANE('',#4841);
#700=FACE_OUTER_BOUND('',#910,.T.);
#701=FACE_OUTER_BOUND('',#911,.T.);
#702=FACE_OUTER_BOUND('',#912,.T.);
#703=FACE_OUTER_BOUND('',#914,.T.);
#704=FACE_OUTER_BOUND('',#915,.T.);
#705=FACE_OUTER_BOUND('',#916,.T.);
#706=FACE_OUTER_BOUND('',#917,.T.);
#707=FACE_OUTER_BOUND('',#919,.T.);
#910=EDGE_LOOP('',(#3177,#3178,#3179,#3180));
#911=EDGE_LOOP('',(#3181,#3182,#3183,#3184));
#912=EDGE_LOOP('',(#3185));
#913=EDGE_LOOP('',(#3186));
#914=EDGE_LOOP('',(#3187,#3188,#3189,#3190));
#915=EDGE_LOOP('',(#3191,#3192,#3193,#3194));
#916=EDGE_LOOP('',(#3195,#3196,#3197,#3198));
#917=EDGE_LOOP('',(#3199));
#918=EDGE_LOOP('',(#3200));
#919=EDGE_LOOP('',(#3201,#3202,#3203,#3204));
#1102=LINE('',#6197,#1280);
#1103=LINE('',#6213,#1281);
#1280=VECTOR('',#5449,19.5);
#1281=VECTOR('',#5472,20.5);
#1445=CIRCLE('',#4826,19.5);
#1446=CIRCLE('',#4827,19.5);
#1447=CIRCLE('',#4829,19.9);
#1448=CIRCLE('',#4830,0.400000000000003);
#1449=CIRCLE('',#4832,20.1);
#1450=CIRCLE('',#4834,20.5);
#1451=CIRCLE('',#4835,0.399999999999996);
#1452=CIRCLE('',#4837,20.5);
#1453=CIRCLE('',#4839,20.1);
#1454=CIRCLE('',#4840,0.399999999999998);
#1455=CIRCLE('',#4842,19.9);
#1456=CIRCLE('',#4844,0.400000000000003);
#1584=VERTEX_POINT('',#6194);
#1585=VERTEX_POINT('',#6196);
#1586=VERTEX_POINT('',#6200);
#1587=VERTEX_POINT('',#6204);
#1588=VERTEX_POINT('',#6207);
#1589=VERTEX_POINT('',#6211);
#1590=VERTEX_POINT('',#6215);
#1591=VERTEX_POINT('',#6219);
#2232=EDGE_CURVE('',#1584,#1584,#1445,.T.);
#2233=EDGE_CURVE('',#1584,#1585,#1102,.T.);
#2234=EDGE_CURVE('',#1585,#1585,#1446,.T.);
#2235=EDGE_CURVE('',#1586,#1586,#1447,.T.);
#2236=EDGE_CURVE('',#1586,#1584,#1448,.T.);
#2237=EDGE_CURVE('',#1587,#1587,#1449,.T.);
#2238=EDGE_CURVE('',#1588,#1588,#1450,.T.);
#2239=EDGE_CURVE('',#1588,#1587,#1451,.T.);
#2240=EDGE_CURVE('',#1589,#1589,#1452,.T.);
#2241=EDGE_CURVE('',#1589,#1588,#1103,.T.);
#2242=EDGE_CURVE('',#1590,#1590,#1453,.T.);
#2243=EDGE_CURVE('',#1590,#1589,#1454,.T.);
#2244=EDGE_CURVE('',#1591,#1591,#1455,.T.);
#2245=EDGE_CURVE('',#1585,#1591,#1456,.T.);
#3177=ORIENTED_EDGE('',*,*,#2232,.F.);
#3178=ORIENTED_EDGE('',*,*,#2233,.T.);
#3179=ORIENTED_EDGE('',*,*,#2234,.T.);
#3180=ORIENTED_EDGE('',*,*,#2233,.F.);
#3181=ORIENTED_EDGE('',*,*,#2235,.F.);
#3182=ORIENTED_EDGE('',*,*,#2236,.T.);
#3183=ORIENTED_EDGE('',*,*,#2232,.T.);
#3184=ORIENTED_EDGE('',*,*,#2236,.F.);
#3185=ORIENTED_EDGE('',*,*,#2237,.F.);
#3186=ORIENTED_EDGE('',*,*,#2235,.T.);
#3187=ORIENTED_EDGE('',*,*,#2238,.F.);
#3188=ORIENTED_EDGE('',*,*,#2239,.T.);
#3189=ORIENTED_EDGE('',*,*,#2237,.T.);
#3190=ORIENTED_EDGE('',*,*,#2239,.F.);
#3191=ORIENTED_EDGE('',*,*,#2240,.F.);
#3192=ORIENTED_EDGE('',*,*,#2241,.T.);
#3193=ORIENTED_EDGE('',*,*,#2238,.T.);
#3194=ORIENTED_EDGE('',*,*,#2241,.F.);
#3195=ORIENTED_EDGE('',*,*,#2242,.F.);
#3196=ORIENTED_EDGE('',*,*,#2243,.T.);
#3197=ORIENTED_EDGE('',*,*,#2240,.T.);
#3198=ORIENTED_EDGE('',*,*,#2243,.F.);
#3199=ORIENTED_EDGE('',*,*,#2242,.T.);
#3200=ORIENTED_EDGE('',*,*,#2244,.F.);
#3201=ORIENTED_EDGE('',*,*,#2234,.F.);
#3202=ORIENTED_EDGE('',*,*,#2245,.T.);
#3203=ORIENTED_EDGE('',*,*,#2244,.T.);
#3204=ORIENTED_EDGE('',*,*,#2245,.F.);
#4299=CYLINDRICAL_SURFACE('',#4825,19.5);
#4300=CYLINDRICAL_SURFACE('',#4836,20.5);
#4475=ADVANCED_FACE('',(#700),#4299,.F.);
#4476=ADVANCED_FACE('',(#701),#522,.T.);
#4477=ADVANCED_FACE('',(#702,#582),#608,.T.);
#4478=ADVANCED_FACE('',(#703),#523,.T.);
#4479=ADVANCED_FACE('',(#704),#4300,.T.);
#4480=ADVANCED_FACE('',(#705),#524,.T.);
#4481=ADVANCED_FACE('',(#706,#583),#609,.T.);
#4482=ADVANCED_FACE('',(#707),#525,.T.);
#4575=CLOSED_SHELL('',(#4475,#4476,#4477,#4478,#4479,#4480,#4481,#4482));
#4824=AXIS2_PLACEMENT_3D('',#6192,#5443,#5444);
#4825=AXIS2_PLACEMENT_3D('',#6193,#5445,#5446);
#4826=AXIS2_PLACEMENT_3D('',#6195,#5447,#5448);
#4827=AXIS2_PLACEMENT_3D('',#6198,#5450,#5451);
#4828=AXIS2_PLACEMENT_3D('',#6199,#5452,#5453);
#4829=AXIS2_PLACEMENT_3D('',#6201,#5454,#5455);
#4830=AXIS2_PLACEMENT_3D('',#6202,#5456,#5457);
#4831=AXIS2_PLACEMENT_3D('',#6203,#5458,#5459);
#4832=AXIS2_PLACEMENT_3D('',#6205,#5460,#5461);
#4833=AXIS2_PLACEMENT_3D('',#6206,#5462,#5463);
#4834=AXIS2_PLACEMENT_3D('',#6208,#5464,#5465);
#4835=AXIS2_PLACEMENT_3D('',#6209,#5466,#5467);
#4836=AXIS2_PLACEMENT_3D('',#6210,#5468,#5469);
#4837=AXIS2_PLACEMENT_3D('',#6212,#5470,#5471);
#4838=AXIS2_PLACEMENT_3D('',#6214,#5473,#5474);
#4839=AXIS2_PLACEMENT_3D('',#6216,#5475,#5476);
#4840=AXIS2_PLACEMENT_3D('',#6217,#5477,#5478);
#4841=AXIS2_PLACEMENT_3D('',#6218,#5479,#5480);
#4842=AXIS2_PLACEMENT_3D('',#6220,#5481,#5482);
#4843=AXIS2_PLACEMENT_3D('',#6221,#5483,#5484);
#4844=AXIS2_PLACEMENT_3D('',#6222,#5485,#5486);
#5443=DIRECTION('axis',(0.,0.,1.));
#5444=DIRECTION('refdir',(1.,0.,0.));
#5445=DIRECTION('center_axis',(0.,0.,1.));
#5446=DIRECTION('ref_axis',(1.,0.,0.));
#5447=DIRECTION('center_axis',(0.,0.,1.));
#5448=DIRECTION('ref_axis',(1.,0.,0.));
#5449=DIRECTION('',(0.,0.,1.));
#5450=DIRECTION('center_axis',(0.,0.,1.));
#5451=DIRECTION('ref_axis',(1.,0.,0.));
#5452=DIRECTION('center_axis',(0.,0.,1.));
#5453=DIRECTION('ref_axis',(1.,0.,0.));
#5454=DIRECTION('center_axis',(0.,0.,1.));
#5455=DIRECTION('ref_axis',(1.,0.,0.));
#5456=DIRECTION('center_axis',(1.22464679914735E-16,-1.,0.));
#5457=DIRECTION('ref_axis',(-1.,-1.22464679914735E-16,0.));
#5458=DIRECTION('center_axis',(0.,0.,-1.));
#5459=DIRECTION('ref_axis',(-1.,0.,0.));
#5460=DIRECTION('center_axis',(0.,0.,1.));
#5461=DIRECTION('ref_axis',(1.,0.,0.));
#5462=DIRECTION('center_axis',(0.,0.,1.));
#5463=DIRECTION('ref_axis',(1.,0.,0.));
#5464=DIRECTION('center_axis',(0.,0.,1.));
#5465=DIRECTION('ref_axis',(1.,0.,0.));
#5466=DIRECTION('center_axis',(1.22464679914735E-16,-1.,0.));
#5467=DIRECTION('ref_axis',(-1.,-1.22464679914735E-16,0.));
#5468=DIRECTION('center_axis',(0.,0.,1.));
#5469=DIRECTION('ref_axis',(1.,0.,0.));
#5470=DIRECTION('center_axis',(0.,0.,1.));
#5471=DIRECTION('ref_axis',(1.,0.,0.));
#5472=DIRECTION('',(0.,0.,-1.));
#5473=DIRECTION('center_axis',(0.,0.,1.));
#5474=DIRECTION('ref_axis',(1.,0.,0.));
#5475=DIRECTION('center_axis',(0.,0.,1.));
#5476=DIRECTION('ref_axis',(1.,0.,0.));
#5477=DIRECTION('center_axis',(1.22464679914735E-16,-1.,0.));
#5478=DIRECTION('ref_axis',(-1.,-1.22464679914735E-16,0.));
#5479=DIRECTION('center_axis',(0.,0.,1.));
#5480=DIRECTION('ref_axis',(1.,0.,0.));
#5481=DIRECTION('center_axis',(0.,0.,1.));
#5482=DIRECTION('ref_axis',(1.,0.,0.));
#5483=DIRECTION('center_axis',(0.,0.,1.));
#5484=DIRECTION('ref_axis',(1.,0.,0.));
#5485=DIRECTION('center_axis',(1.22464679914735E-16,-1.,0.));
#5486=DIRECTION('ref_axis',(-1.,-1.22464679914735E-16,0.));
#6192=CARTESIAN_POINT('',(0.,0.,0.));
#6193=CARTESIAN_POINT('Origin',(0.,0.,4.));
#6194=CARTESIAN_POINT('',(-19.5,-2.38806125833734E-15,2.9));
#6195=CARTESIAN_POINT('Origin',(0.,0.,2.9));
#6196=CARTESIAN_POINT('',(-19.5,-2.38806125833734E-15,5.1));
#6197=CARTESIAN_POINT('',(-19.5,-2.38806125833734E-15,4.));
#6198=CARTESIAN_POINT('Origin',(0.,0.,5.1));
#6199=CARTESIAN_POINT('Origin',(0.,0.,2.9));
#6200=CARTESIAN_POINT('',(-19.9,-2.43704713030323E-15,2.5));
#6201=CARTESIAN_POINT('Origin',(0.,0.,2.5));
#6202=CARTESIAN_POINT('Origin',(-19.9,-2.43704713030323E-15,2.9));
#6203=CARTESIAN_POINT('Origin',(20.1,0.,2.5));
#6204=CARTESIAN_POINT('',(-20.1,-2.46154006628618E-15,2.5));
#6205=CARTESIAN_POINT('Origin',(0.,0.,2.5));
#6206=CARTESIAN_POINT('Origin',(0.,0.,2.9));
#6207=CARTESIAN_POINT('',(-20.5,-2.51052593825207E-15,2.9));
#6208=CARTESIAN_POINT('Origin',(0.,0.,2.9));
#6209=CARTESIAN_POINT('Origin',(-20.1,-2.46154006628618E-15,2.9));
#6210=CARTESIAN_POINT('Origin',(0.,0.,4.));
#6211=CARTESIAN_POINT('',(-20.5,-2.51052593825207E-15,5.1));
#6212=CARTESIAN_POINT('Origin',(0.,0.,5.1));
#6213=CARTESIAN_POINT('',(-20.5,-2.51052593825207E-15,4.));
#6214=CARTESIAN_POINT('Origin',(0.,0.,5.1));
#6215=CARTESIAN_POINT('',(-20.1,-2.46154006628618E-15,5.5));
#6216=CARTESIAN_POINT('Origin',(0.,0.,5.5));
#6217=CARTESIAN_POINT('Origin',(-20.1,-2.46154006628618E-15,5.1));
#6218=CARTESIAN_POINT('Origin',(19.9,0.,5.5));
#6219=CARTESIAN_POINT('',(-19.9,-2.43704713030323E-15,5.5));
#6220=CARTESIAN_POINT('Origin',(0.,0.,5.5));
#6221=CARTESIAN_POINT('Origin',(0.,0.,5.1));
#6222=CARTESIAN_POINT('Origin',(-19.9,-2.43704713030323E-15,5.1));
#74095=UNCERTAINTY_MEASURE_WITH_UNIT(LENGTH_MEASURE(0.01),#74104,
'DISTANCE_ACCURACY_VALUE',
'Maximum model space distance between geometric entities at asserted c
onnectivities');
#74097=UNCERTAINTY_MEASURE_WITH_UNIT(LENGTH_MEASURE(0.01),#74104,
'DISTANCE_ACCURACY_VALUE',
'Maximum model space distance between geometric entities at asserted c
onnectivities');
#74101=(
GEOMETRIC_REPRESENTATION_CONTEXT(3)
GLOBAL_UNCERTAINTY_ASSIGNED_CONTEXT((#74095))
GLOBAL_UNIT_ASSIGNED_CONTEXT((#74104,#74106,#74107))
REPRESENTATION_CONTEXT('','3D')
);
#74103=(
GEOMETRIC_REPRESENTATION_CONTEXT(3)
GLOBAL_UNCERTAINTY_ASSIGNED_CONTEXT((#74097))
GLOBAL_UNIT_ASSIGNED_CONTEXT((#74104,#74106,#74107))
REPRESENTATION_CONTEXT('','3D')
);
#74104=(
LENGTH_UNIT()
NAMED_UNIT(*)
SI_UNIT(.MILLI.,.METRE.)
);
#74106=(
NAMED_UNIT(*)
PLANE_ANGLE_UNIT()
SI_UNIT($,.RADIAN.)
);
#74107=(
NAMED_UNIT(*)
SI_UNIT($,.STERADIAN.)
SOLID_ANGLE_UNIT()
);
#74111=SHAPE_DEFINITION_REPRESENTATION(#74116,#74130);
#74116=PRODUCT_DEFINITION_SHAPE('',$,#74136);
#74130=SHAPE_REPRESENTATION('',(#4824),#74101);
#74132=PRODUCT_DEFINITION_CONTEXT('part definition',#74149,'design');
#74136=PRODUCT_DEFINITION('Ring_01','Ring_01',#74141,#74132);
#74141=PRODUCT_DEFINITION_FORMATION('',$,#74154);
#74149=APPLICATION_CONTEXT(
'Core Data for Automotive Mechanical Design Process');
#74150=PRODUCT_CONTEXT('part definition',#74149,'mechanical');
#74154=PRODUCT('Ring_01','Ring_01',$,(#74150));
#74158=PRESENTATION_STYLE_ASSIGNMENT((#74162));
#74162=SURFACE_STYLE_USAGE(.BOTH.,#74166);
#74166=SURFACE_SIDE_STYLE('',(#74170));
#74170=SURFACE_STYLE_FILL_AREA(#74174);
#74174=FILL_AREA_STYLE('Opaque(52,52,60)',(#74178));
#74178=FILL_AREA_STYLE_COLOUR('Opaque(52,52,60)',#74182);
#74182=COLOUR_RGB('Opaque(52,52,60)', 0.31764706, 0.68627451, 0.89019608);
ENDSEC;
END-ISO-10303-21;
